ISO-10303-21;
HEADER;
/* Generated by software containing ST-Developer
 * from STEP Tools, Inc. (www.steptools.com) 
 */

FILE_DESCRIPTION(
/* description */ (''),
/* implementation_level */ '2;1');

FILE_NAME(
/* name */ 'Screw_01.step',
/* time_stamp */ '2026-10-06T13:23:02-07:00',
/* author */ (''),
/* organization */ (''),
/* preprocessor_version */ 'ST-DEVELOPER v20.2',
/* originating_system */ 'Autodesk Translation Framework v15.15.0.0',
/* authorisation */ '');

FILE_SCHEMA (('AUTOMOTIVE_DESIGN { 1 0 10303 214 3 1 1 }'));
ENDSEC;

DATA;
#10=MECHANICAL_DESIGN_GEOMETRIC_PRESENTATION_REPRESENTATION('',(#71),#4994);
#51=SHAPE_REPRESENTATION_RELATIONSHIP('SRR','None',#5032,#61);
#61=ADVANCED_BREP_SHAPE_REPRESENTATION('',(#81),#4984);
#71=STYLED_ITEM('',(#5091),#81);
#81=MANIFOLD_SOLID_BREP('Body1',#2911);
#91=CYLINDRICAL_SURFACE('',#3042,1.9);
#92=CYLINDRICAL_SURFACE('',#3056,0.96675);
#123=FACE_BOUND('',#484,.T.);
#124=FACE_BOUND('',#501,.T.);
#166=PLANE('',#3041);
#167=PLANE('',#3044);
#168=PLANE('',#3045);
#169=PLANE('',#3046);
#170=PLANE('',#3047);
#171=PLANE('',#3048);
#172=PLANE('',#3049);
#173=PLANE('',#3050);
#174=PLANE('',#3051);
#175=PLANE('',#3052);
#176=PLANE('',#3053);
#177=PLANE('',#3054);
#178=PLANE('',#3055);
#179=PLANE('',#3058);
#180=PLANE('',#3059);
#299=TOROIDAL_SURFACE('',#3037,1.7,0.2);
#303=FACE_OUTER_BOUND('',#481,.T.);
#304=FACE_OUTER_BOUND('',#482,.T.);
#305=FACE_OUTER_BOUND('',#483,.T.);
#306=FACE_OUTER_BOUND('',#485,.T.);
#307=FACE_OUTER_BOUND('',#486,.T.);
#308=FACE_OUTER_BOUND('',#487,.T.);
#309=FACE_OUTER_BOUND('',#488,.T.);
#310=FACE_OUTER_BOUND('',#489,.T.);
#311=FACE_OUTER_BOUND('',#490,.T.);
#312=FACE_OUTER_BOUND('',#491,.T.);
#313=FACE_OUTER_BOUND('',#492,.T.);
#314=FACE_OUTER_BOUND('',#493,.T.);
#315=FACE_OUTER_BOUND('',#494,.T.);
#316=FACE_OUTER_BOUND('',#495,.T.);
#317=FACE_OUTER_BOUND('',#496,.T.);
#318=FACE_OUTER_BOUND('',#497,.T.);
#319=FACE_OUTER_BOUND('',#498,.T.);
#320=FACE_OUTER_BOUND('',#499,.T.);
#321=FACE_OUTER_BOUND('',#500,.T.);
#481=EDGE_LOOP('',(#1976,#1977,#1978,#1979));
#482=EDGE_LOOP('',(#1980,#1981,#1982,#1983));
#483=EDGE_LOOP('',(#1984));
#484=EDGE_LOOP('',(#1985,#1986,#1987,#1988,#1989,#1990));
#485=EDGE_LOOP('',(#1991,#1992,#1993,#1994));
#486=EDGE_LOOP('',(#1995,#1996,#1997));
#487=EDGE_LOOP('',(#1998,#1999,#2000));
#488=EDGE_LOOP('',(#2001,#2002,#2003));
#489=EDGE_LOOP('',(#2004,#2005,#2006));
#490=EDGE_LOOP('',(#2007,#2008,#2009));
#491=EDGE_LOOP('',(#2010,#2011,#2012));
#492=EDGE_LOOP('',(#2013,#2014,#2015,#2016));
#493=EDGE_LOOP('',(#2017,#2018,#2019,#2020));
#494=EDGE_LOOP('',(#2021,#2022,#2023,#2024));
#495=EDGE_LOOP('',(#2025,#2026,#2027,#2028));
#496=EDGE_LOOP('',(#2029,#2030,#2031,#2032));
#497=EDGE_LOOP('',(#2033,#2034,#2035,#2036));
#498=EDGE_LOOP('',(#2037,#2038,#2039,#2040));
#499=EDGE_LOOP('',(#2041));
#500=EDGE_LOOP('',(#2042));
#501=EDGE_LOOP('',(#2043));
#702=LINE('',#4171,#995);
#703=LINE('',#4182,#996);
#704=LINE('',#4184,#997);
#705=LINE('',#4186,#998);
#706=LINE('',#4188,#999);
#707=LINE('',#4190,#1000);
#708=LINE('',#4191,#1001);
#709=LINE('',#4195,#1002);
#710=LINE('',#4199,#1003);
#711=LINE('',#4201,#1004);
#712=LINE('',#4202,#1005);
#713=LINE('',#4205,#1006);
#714=LINE('',#4206,#1007);
#715=LINE('',#4209,#1008);
#716=LINE('',#4210,#1009);
#717=LINE('',#4213,#1010);
#718=LINE('',#4214,#1011);
#719=LINE('',#4217,#1012);
#720=LINE('',#4218,#1013);
#721=LINE('',#4220,#1014);
#722=LINE('',#4222,#1015);
#723=LINE('',#4223,#1016);
#724=LINE('',#4225,#1017);
#725=LINE('',#4227,#1018);
#726=LINE('',#4229,#1019);
#727=LINE('',#4231,#1020);
#728=LINE('',#4235,#1021);
#995=VECTOR('',#3320,0.887310000000001);
#996=VECTOR('',#3333,10.);
#997=VECTOR('',#3334,10.);
#998=VECTOR('',#3335,10.);
#999=VECTOR('',#3336,10.);
#1000=VECTOR('',#3337,10.);
#1001=VECTOR('',#3338,10.);
#1002=VECTOR('',#3343,1.9);
#1003=VECTOR('',#3346,9.99999999999999);
#1004=VECTOR('',#3347,10.);
#1005=VECTOR('',#3348,10.);
#1006=VECTOR('',#3351,10.);
#1007=VECTOR('',#3352,10.);
#1008=VECTOR('',#3355,10.);
#1009=VECTOR('',#3356,9.99999999999999);
#1010=VECTOR('',#3359,10.);
#1011=VECTOR('',#3360,10.);
#1012=VECTOR('',#3363,10.);
#1013=VECTOR('',#3364,10.);
#1014=VECTOR('',#3367,10.);
#1015=VECTOR('',#3370,10.);
#1016=VECTOR('',#3371,10.);
#1017=VECTOR('',#3374,10.);
#1018=VECTOR('',#3377,10.);
#1019=VECTOR('',#3380,10.);
#1020=VECTOR('',#3383,10.);
#1021=VECTOR('',#3388,0.96675);
#1288=CIRCLE('',#3035,0.96675);
#1289=CIRCLE('',#3036,0.754619999999998);
#1290=CIRCLE('',#3038,1.9);
#1291=CIRCLE('',#3039,0.2);
#1292=CIRCLE('',#3040,1.7);
#1293=CIRCLE('',#3043,1.9);
#1294=CIRCLE('',#3057,0.96675);
#1369=VERTEX_POINT('',#4168);
#1370=VERTEX_POINT('',#4170);
#1371=VERTEX_POINT('',#4174);
#1372=VERTEX_POINT('',#4176);
#1373=VERTEX_POINT('',#4180);
#1374=VERTEX_POINT('',#4181);
#1375=VERTEX_POINT('',#4183);
#1376=VERTEX_POINT('',#4185);
#1377=VERTEX_POINT('',#4187);
#1378=VERTEX_POINT('',#4189);
#1379=VERTEX_POINT('',#4193);
#1380=VERTEX_POINT('',#4197);
#1381=VERTEX_POINT('',#4198);
#1382=VERTEX_POINT('',#4200);
#1383=VERTEX_POINT('',#4204);
#1384=VERTEX_POINT('',#4208);
#1385=VERTEX_POINT('',#4212);
#1386=VERTEX_POINT('',#4216);
#1387=VERTEX_POINT('',#4234);
#1602=EDGE_CURVE('',#1369,#1369,#1288,.T.);
#1603=EDGE_CURVE('',#1369,#1370,#702,.T.);
#1604=EDGE_CURVE('',#1370,#1370,#1289,.T.);
#1605=EDGE_CURVE('',#1371,#1371,#1290,.T.);
#1606=EDGE_CURVE('',#1371,#1372,#1291,.T.);
#1607=EDGE_CURVE('',#1372,#1372,#1292,.T.);
#1608=EDGE_CURVE('',#1373,#1374,#703,.T.);
#1609=EDGE_CURVE('',#1374,#1375,#704,.T.);
#1610=EDGE_CURVE('',#1375,#1376,#705,.T.);
#1611=EDGE_CURVE('',#1376,#1377,#706,.T.);
#1612=EDGE_CURVE('',#1377,#1378,#707,.T.);
#1613=EDGE_CURVE('',#1378,#1373,#708,.T.);
#1614=EDGE_CURVE('',#1379,#1379,#1293,.T.);
#1615=EDGE_CURVE('',#1379,#1371,#709,.T.);
#1616=EDGE_CURVE('',#1380,#1381,#710,.T.);
#1617=EDGE_CURVE('',#1382,#1380,#711,.T.);
#1618=EDGE_CURVE('',#1382,#1381,#712,.T.);
#1619=EDGE_CURVE('',#1383,#1382,#713,.T.);
#1620=EDGE_CURVE('',#1383,#1381,#714,.T.);
#1621=EDGE_CURVE('',#1384,#1383,#715,.T.);
#1622=EDGE_CURVE('',#1384,#1381,#716,.T.);
#1623=EDGE_CURVE('',#1385,#1384,#717,.T.);
#1624=EDGE_CURVE('',#1385,#1381,#718,.T.);
#1625=EDGE_CURVE('',#1386,#1385,#719,.T.);
#1626=EDGE_CURVE('',#1386,#1381,#720,.T.);
#1627=EDGE_CURVE('',#1380,#1386,#721,.T.);
#1628=EDGE_CURVE('',#1373,#1382,#722,.T.);
#1629=EDGE_CURVE('',#1374,#1380,#723,.T.);
#1630=EDGE_CURVE('',#1378,#1383,#724,.T.);
#1631=EDGE_CURVE('',#1377,#1384,#725,.T.);
#1632=EDGE_CURVE('',#1376,#1385,#726,.T.);
#1633=EDGE_CURVE('',#1375,#1386,#727,.T.);
#1634=EDGE_CURVE('',#1369,#1387,#728,.T.);
#1635=EDGE_CURVE('',#1387,#1387,#1294,.F.);
#1976=ORIENTED_EDGE('',*,*,#1602,.F.);
#1977=ORIENTED_EDGE('',*,*,#1603,.T.);
#1978=ORIENTED_EDGE('',*,*,#1604,.F.);
#1979=ORIENTED_EDGE('',*,*,#1603,.F.);
#1980=ORIENTED_EDGE('',*,*,#1605,.T.);
#1981=ORIENTED_EDGE('',*,*,#1606,.T.);
#1982=ORIENTED_EDGE('',*,*,#1607,.T.);
#1983=ORIENTED_EDGE('',*,*,#1606,.F.);
#1984=ORIENTED_EDGE('',*,*,#1607,.F.);
#1985=ORIENTED_EDGE('',*,*,#1608,.T.);
#1986=ORIENTED_EDGE('',*,*,#1609,.T.);
#1987=ORIENTED_EDGE('',*,*,#1610,.T.);
#1988=ORIENTED_EDGE('',*,*,#1611,.T.);
#1989=ORIENTED_EDGE('',*,*,#1612,.T.);
#1990=ORIENTED_EDGE('',*,*,#1613,.T.);
#1991=ORIENTED_EDGE('',*,*,#1614,.F.);
#1992=ORIENTED_EDGE('',*,*,#1615,.T.);
#1993=ORIENTED_EDGE('',*,*,#1605,.F.);
#1994=ORIENTED_EDGE('',*,*,#1615,.F.);
#1995=ORIENTED_EDGE('',*,*,#1616,.F.);
#1996=ORIENTED_EDGE('',*,*,#1617,.F.);
#1997=ORIENTED_EDGE('',*,*,#1618,.T.);
#1998=ORIENTED_EDGE('',*,*,#1618,.F.);
#1999=ORIENTED_EDGE('',*,*,#1619,.F.);
#2000=ORIENTED_EDGE('',*,*,#1620,.T.);
#2001=ORIENTED_EDGE('',*,*,#1620,.F.);
#2002=ORIENTED_EDGE('',*,*,#1621,.F.);
#2003=ORIENTED_EDGE('',*,*,#1622,.T.);
#2004=ORIENTED_EDGE('',*,*,#1622,.F.);
#2005=ORIENTED_EDGE('',*,*,#1623,.F.);
#2006=ORIENTED_EDGE('',*,*,#1624,.T.);
#2007=ORIENTED_EDGE('',*,*,#1624,.F.);
#2008=ORIENTED_EDGE('',*,*,#1625,.F.);
#2009=ORIENTED_EDGE('',*,*,#1626,.T.);
#2010=ORIENTED_EDGE('',*,*,#1626,.F.);
#2011=ORIENTED_EDGE('',*,*,#1627,.F.);
#2012=ORIENTED_EDGE('',*,*,#1616,.T.);
#2013=ORIENTED_EDGE('',*,*,#1608,.F.);
#2014=ORIENTED_EDGE('',*,*,#1628,.T.);
#2015=ORIENTED_EDGE('',*,*,#1617,.T.);
#2016=ORIENTED_EDGE('',*,*,#1629,.F.);
#2017=ORIENTED_EDGE('',*,*,#1613,.F.);
#2018=ORIENTED_EDGE('',*,*,#1630,.T.);
#2019=ORIENTED_EDGE('',*,*,#1619,.T.);
#2020=ORIENTED_EDGE('',*,*,#1628,.F.);
#2021=ORIENTED_EDGE('',*,*,#1612,.F.);
#2022=ORIENTED_EDGE('',*,*,#1631,.T.);
#2023=ORIENTED_EDGE('',*,*,#1621,.T.);
#2024=ORIENTED_EDGE('',*,*,#1630,.F.);
#2025=ORIENTED_EDGE('',*,*,#1611,.F.);
#2026=ORIENTED_EDGE('',*,*,#1632,.T.);
#2027=ORIENTED_EDGE('',*,*,#1623,.T.);
#2028=ORIENTED_EDGE('',*,*,#1631,.F.);
#2029=ORIENTED_EDGE('',*,*,#1610,.F.);
#2030=ORIENTED_EDGE('',*,*,#1633,.T.);
#2031=ORIENTED_EDGE('',*,*,#1625,.T.);
#2032=ORIENTED_EDGE('',*,*,#1632,.F.);
#2033=ORIENTED_EDGE('',*,*,#1609,.F.);
#2034=ORIENTED_EDGE('',*,*,#1629,.T.);
#2035=ORIENTED_EDGE('',*,*,#1627,.T.);
#2036=ORIENTED_EDGE('',*,*,#1633,.F.);
#2037=ORIENTED_EDGE('',*,*,#1602,.T.);
#2038=ORIENTED_EDGE('',*,*,#1634,.T.);
#2039=ORIENTED_EDGE('',*,*,#1635,.T.);
#2040=ORIENTED_EDGE('',*,*,#1634,.F.);
#2041=ORIENTED_EDGE('',*,*,#1604,.T.);
#2042=ORIENTED_EDGE('',*,*,#1614,.T.);
#2043=ORIENTED_EDGE('',*,*,#1635,.F.);
#2724=CONICAL_SURFACE('',#3034,0.887310000000001,0.824535502685815);
#2733=ADVANCED_FACE('',(#303),#2724,.T.);
#2734=ADVANCED_FACE('',(#304),#299,.T.);
#2735=ADVANCED_FACE('',(#305,#123),#166,.T.);
#2736=ADVANCED_FACE('',(#306),#91,.T.);
#2737=ADVANCED_FACE('',(#307),#167,.F.);
#2738=ADVANCED_FACE('',(#308),#168,.F.);
#2739=ADVANCED_FACE('',(#309),#169,.F.);
#2740=ADVANCED_FACE('',(#310),#170,.F.);
#2741=ADVANCED_FACE('',(#311),#171,.F.);
#2742=ADVANCED_FACE('',(#312),#172,.F.);
#2743=ADVANCED_FACE('',(#313),#173,.F.);
#2744=ADVANCED_FACE('',(#314),#174,.F.);
#2745=ADVANCED_FACE('',(#315),#175,.F.);
#2746=ADVANCED_FACE('',(#316),#176,.F.);
#2747=ADVANCED_FACE('',(#317),#177,.F.);
#2748=ADVANCED_FACE('',(#318),#178,.F.);
#2749=ADVANCED_FACE('',(#319),#92,.T.);
#2750=ADVANCED_FACE('',(#320),#179,.T.);
#2751=ADVANCED_FACE('',(#321,#124),#180,.T.);
#2911=CLOSED_SHELL('',(#2733,#2734,#2735,#2736,#2737,#2738,#2739,#2740,
#2741,#2742,#2743,#2744,#2745,#2746,#2747,#2748,#2749,#2750,#2751));
#3033=AXIS2_PLACEMENT_3D('',#4166,#3314,#3315);
#3034=AXIS2_PLACEMENT_3D('',#4167,#3316,#3317);
#3035=AXIS2_PLACEMENT_3D('',#4169,#3318,#3319);
#3036=AXIS2_PLACEMENT_3D('',#4172,#3321,#3322);
#3037=AXIS2_PLACEMENT_3D('',#4173,#3323,#3324);
#3038=AXIS2_PLACEMENT_3D('',#4175,#3325,#3326);
#3039=AXIS2_PLACEMENT_3D('',#4177,#3327,#3328);
#3040=AXIS2_PLACEMENT_3D('',#4178,#3329,#3330);
#3041=AXIS2_PLACEMENT_3D('',#4179,#3331,#3332);
#3042=AXIS2_PLACEMENT_3D('',#4192,#3339,#3340);
#3043=AXIS2_PLACEMENT_3D('',#4194,#3341,#3342);
#3044=AXIS2_PLACEMENT_3D('',#4196,#3344,#3345);
#3045=AXIS2_PLACEMENT_3D('',#4203,#3349,#3350);
#3046=AXIS2_PLACEMENT_3D('',#4207,#3353,#3354);
#3047=AXIS2_PLACEMENT_3D('',#4211,#3357,#3358);
#3048=AXIS2_PLACEMENT_3D('',#4215,#3361,#3362);
#3049=AXIS2_PLACEMENT_3D('',#4219,#3365,#3366);
#3050=AXIS2_PLACEMENT_3D('',#4221,#3368,#3369);
#3051=AXIS2_PLACEMENT_3D('',#4224,#3372,#3373);
#3052=AXIS2_PLACEMENT_3D('',#4226,#3375,#3376);
#3053=AXIS2_PLACEMENT_3D('',#4228,#3378,#3379);
#3054=AXIS2_PLACEMENT_3D('',#4230,#3381,#3382);
#3055=AXIS2_PLACEMENT_3D('',#4232,#3384,#3385);
#3056=AXIS2_PLACEMENT_3D('',#4233,#3386,#3387);
#3057=AXIS2_PLACEMENT_3D('',#4236,#3389,#3390);
#3058=AXIS2_PLACEMENT_3D('',#4237,#3391,#3392);
#3059=AXIS2_PLACEMENT_3D('',#4238,#3393,#3394);
#3314=DIRECTION('axis',(0.,0.,1.));
#3315=DIRECTION('refdir',(1.,0.,0.));
#3316=DIRECTION('center_axis',(0.,0.,1.));
#3317=DIRECTION('ref_axis',(-1.,0.,0.));
#3318=DIRECTION('center_axis',(-1.06387651071382E-15,0.,1.));
#3319=DIRECTION('ref_axis',(-1.,0.,-1.06387651071382E-15));
#3320=DIRECTION('',(-0.73423251512767,-8.99175499481012E-17,-0.678898087881602));
#3321=DIRECTION('center_axis',(1.06387651071382E-15,0.,-1.));
#3322=DIRECTION('ref_axis',(-1.,0.,-1.06387651071382E-15));
#3323=DIRECTION('center_axis',(1.06387651071382E-15,0.,-1.));
#3324=DIRECTION('ref_axis',(-1.,0.,-1.05179023385541E-15));
#3325=DIRECTION('center_axis',(-1.06387651071382E-15,0.,1.));
#3326=DIRECTION('ref_axis',(1.,0.,1.06387651071382E-15));
#3327=DIRECTION('center_axis',(-1.22464679914735E-16,-1.,-1.30287296353373E-31));
#3328=DIRECTION('ref_axis',(1.,-1.22464679914735E-16,1.02257383847054E-15));
#3329=DIRECTION('center_axis',(1.06387651071382E-15,0.,-1.));
#3330=DIRECTION('ref_axis',(1.,0.,1.06387651071382E-15));
#3331=DIRECTION('center_axis',(-1.06387651071382E-15,0.,1.));
#3332=DIRECTION('ref_axis',(1.,0.,1.06387651071382E-15));
#3333=DIRECTION('',(-0.866025403784439,-0.5,-9.21344084767719E-16));
#3334=DIRECTION('',(-0.866025403784439,0.5,-9.21344084767719E-16));
#3335=DIRECTION('',(6.40987562127854E-16,1.,6.81931611007542E-31));
#3336=DIRECTION('',(0.866025403784439,0.5,9.21344084767719E-16));
#3337=DIRECTION('',(0.866025403784439,-0.5,9.21344084767719E-16));
#3338=DIRECTION('',(-1.60246890531964E-16,-1.,-1.70482902751885E-31));
#3339=DIRECTION('center_axis',(1.06387651071382E-15,0.,-1.));
#3340=DIRECTION('ref_axis',(-1.,0.,-1.06387651071382E-15));
#3341=DIRECTION('center_axis',(1.06387651071382E-15,0.,-1.));
#3342=DIRECTION('ref_axis',(1.,0.,1.06387651071382E-15));
#3343=DIRECTION('',(-1.06387651071382E-15,0.,1.));
#3344=DIRECTION('center_axis',(0.0435778713738291,-0.0754790873051733,-0.996194698091746));
#3345=DIRECTION('ref_axis',(-0.866025403784439,-0.5,-3.35810244624808E-17));
#3346=DIRECTION('',(0.,0.997141949694316,-0.0755508581011305));
#3347=DIRECTION('',(-0.866025403784439,-0.5,0.));
#3348=DIRECTION('',(-0.863550259614423,0.498570974847158,-0.0755508581011305));
#3349=DIRECTION('center_axis',(0.0871557427476581,-1.3966436767316E-17,
-0.996194698091746));
#3350=DIRECTION('ref_axis',(-1.60246890531964E-16,-1.,1.77292017095641E-32));
#3351=DIRECTION('',(-1.60246890531964E-16,-1.,0.));
#3352=DIRECTION('',(-0.863550259614423,-0.498570974847158,-0.0755508581011305));
#3353=DIRECTION('center_axis',(0.0435778713738291,0.0754790873051733,-0.996194698091746));
#3354=DIRECTION('ref_axis',(0.866025403784439,-0.5,3.35810244624808E-17));
#3355=DIRECTION('',(0.866025403784439,-0.5,0.));
#3356=DIRECTION('',(-1.59381164582915E-16,-0.997141949694316,-0.0755508581011305));
#3357=DIRECTION('center_axis',(-0.0435778713738291,0.0754790873051733,-0.996194698091746));
#3358=DIRECTION('ref_axis',(0.866025403784439,0.5,-3.35810244624808E-17));
#3359=DIRECTION('',(0.866025403784439,0.5,0.));
#3360=DIRECTION('',(0.863550259614423,-0.498570974847159,-0.0755508581011305));
#3361=DIRECTION('center_axis',(-0.0871557427476581,5.58657470692638E-17,
-0.996194698091746));
#3362=DIRECTION('ref_axis',(6.40987562127854E-16,1.,4.7015367027096E-32));
#3363=DIRECTION('',(6.40987562127854E-16,1.,0.));
#3364=DIRECTION('',(0.863550259614423,0.498570974847158,-0.0755508581011305));
#3365=DIRECTION('center_axis',(-0.0435778713738291,-0.0754790873051733,
-0.996194698091746));
#3366=DIRECTION('ref_axis',(-0.866025403784439,0.5,3.35810244624808E-17));
#3367=DIRECTION('',(-0.866025403784439,0.5,0.));
#3368=DIRECTION('center_axis',(0.5,-0.866025403784439,0.));
#3369=DIRECTION('ref_axis',(-0.866025403784439,-0.5,0.));
#3370=DIRECTION('',(0.,0.,-1.));
#3371=DIRECTION('',(0.,0.,-1.));
#3372=DIRECTION('center_axis',(1.,-1.60246890531964E-16,0.));
#3373=DIRECTION('ref_axis',(-1.60246890531964E-16,-1.,0.));
#3374=DIRECTION('',(0.,0.,-1.));
#3375=DIRECTION('center_axis',(0.5,0.866025403784439,0.));
#3376=DIRECTION('ref_axis',(0.866025403784439,-0.5,0.));
#3377=DIRECTION('',(0.,0.,-1.));
#3378=DIRECTION('center_axis',(-0.5,0.866025403784439,0.));
#3379=DIRECTION('ref_axis',(0.866025403784439,0.5,0.));
#3380=DIRECTION('',(0.,0.,-1.));
#3381=DIRECTION('center_axis',(-1.,6.40987562127854E-16,0.));
#3382=DIRECTION('ref_axis',(6.40987562127854E-16,1.,0.));
#3383=DIRECTION('',(0.,0.,-1.));
#3384=DIRECTION('center_axis',(-0.5,-0.866025403784439,0.));
#3385=DIRECTION('ref_axis',(-0.866025403784439,0.5,0.));
#3386=DIRECTION('center_axis',(1.06387651071382E-15,0.,-1.));
#3387=DIRECTION('ref_axis',(-1.,0.,-1.06387651071382E-15));
#3388=DIRECTION('',(-1.06387651071382E-15,0.,1.));
#3389=DIRECTION('center_axis',(-1.06387651071382E-15,0.,1.));
#3390=DIRECTION('ref_axis',(-1.,0.,-1.06387651071382E-15));
#3391=DIRECTION('center_axis',(1.06387651071382E-15,0.,-1.));
#3392=DIRECTION('ref_axis',(-1.,0.,-1.06387651071382E-15));
#3393=DIRECTION('center_axis',(1.06387651071382E-15,0.,-1.));
#3394=DIRECTION('ref_axis',(-1.,0.,-1.06387651071382E-15));
#4166=CARTESIAN_POINT('',(0.,0.,0.));
#4167=CARTESIAN_POINT('Origin',(0.,0.,-4.87731));
#4168=CARTESIAN_POINT('',(0.966750000000005,1.1839272930757E-16,-4.80385688672847));
#4169=CARTESIAN_POINT('Origin',(5.11071050262126E-15,0.,-4.80385688672847));
#4170=CARTESIAN_POINT('',(0.754619999999998,-9.24142967572573E-17,-5.));
#4171=CARTESIAN_POINT('',(0.887310000000001,1.08664135135144E-16,-4.87731));
#4172=CARTESIAN_POINT('Origin',(0.,0.,-5.));
#4173=CARTESIAN_POINT('Origin',(-1.91497771928438E-15,0.,1.79999999999952));
#4174=CARTESIAN_POINT('',(1.89999999999999,-2.32682891837997E-16,1.79999999999953));
#4175=CARTESIAN_POINT('Origin',(-1.91497771928438E-15,0.,1.79999999999952));
#4176=CARTESIAN_POINT('',(1.69999999999999,-2.0818995585505E-16,1.99999999999953));
#4177=CARTESIAN_POINT('Origin',(1.7,-2.0818995585505E-16,1.79999999999952));
#4178=CARTESIAN_POINT('Origin',(-2.12775302142714E-15,0.,1.99999999999952));
#4179=CARTESIAN_POINT('Origin',(-1.9,0.,1.99999999999952));
#4180=CARTESIAN_POINT('',(0.75,-0.433012701892219,2.));
#4181=CARTESIAN_POINT('',(1.38777878078145E-16,-0.866025403784439,2.));
#4182=CARTESIAN_POINT('',(-0.149999999999999,-0.952627944162883,1.99999999999952));
#4183=CARTESIAN_POINT('',(-0.750000000000001,-0.433012701892219,2.));
#4184=CARTESIAN_POINT('',(-0.899999999999999,-0.346410161513776,1.99999999999952));
#4185=CARTESIAN_POINT('',(-0.75,0.43301270189222,2.));
#4186=CARTESIAN_POINT('',(-0.75,-0.21650635094611,1.99999999999952));
#4187=CARTESIAN_POINT('',(1.73472347597681E-17,0.866025403784439,2.));
#4188=CARTESIAN_POINT('',(-1.275,0.129903810567666,1.99999999999952));
#4189=CARTESIAN_POINT('',(0.75,0.433012701892219,2.));
#4190=CARTESIAN_POINT('',(-0.524999999999999,1.16913429510899,1.99999999999952));
#4191=CARTESIAN_POINT('',(0.75,0.216506350946109,1.99999999999952));
#4192=CARTESIAN_POINT('Origin',(-1.06387651071333E-15,0.,0.999999999999538));
#4193=CARTESIAN_POINT('',(1.9,-2.32682891837997E-16,-4.47419878923938E-13));
#4194=CARTESIAN_POINT('Origin',(4.74691816123085E-28,0.,-4.48558184615945E-13));
#4195=CARTESIAN_POINT('',(1.9,-2.32682891837997E-16,0.99999999999954));
#4196=CARTESIAN_POINT('Origin',(1.38777878078145E-16,-0.866025403784439,
1.));
#4197=CARTESIAN_POINT('',(1.38777878078145E-16,-0.866025403784439,1.));
#4198=CARTESIAN_POINT('',(0.,2.77555756156289E-16,0.934383502355557));
#4199=CARTESIAN_POINT('',(0.,-0.650754856401699,0.983689509218169));
#4200=CARTESIAN_POINT('',(0.75,-0.433012701892219,1.));
#4201=CARTESIAN_POINT('',(8.5846548499269E-17,-0.866025403784439,1.));
#4202=CARTESIAN_POINT('',(0.563570237279966,-0.325377428200849,0.983689509218169));
#4203=CARTESIAN_POINT('Origin',(0.75,-0.433012701892219,1.));
#4204=CARTESIAN_POINT('',(0.75,0.433012701892219,1.));
#4205=CARTESIAN_POINT('',(0.75,-0.433012701892219,1.));
#4206=CARTESIAN_POINT('',(0.563570237279966,0.32537742820085,0.983689509218169));
#4207=CARTESIAN_POINT('Origin',(0.75,0.433012701892219,1.));
#4208=CARTESIAN_POINT('',(0.,0.866025403784439,1.));
#4209=CARTESIAN_POINT('',(0.75,0.433012701892219,1.));
#4210=CARTESIAN_POINT('',(0.,0.650754856401699,0.983689509218169));
#4211=CARTESIAN_POINT('Origin',(0.,0.866025403784439,1.));
#4212=CARTESIAN_POINT('',(-0.75,0.43301270189222,1.));
#4213=CARTESIAN_POINT('',(1.73472347597681E-17,0.866025403784439,1.));
#4214=CARTESIAN_POINT('',(-0.563570237279966,0.325377428200849,0.983689509218169));
#4215=CARTESIAN_POINT('Origin',(-0.75,0.43301270189222,1.));
#4216=CARTESIAN_POINT('',(-0.750000000000001,-0.433012701892219,1.));
#4217=CARTESIAN_POINT('',(-0.75,0.43301270189222,1.));
#4218=CARTESIAN_POINT('',(-0.563570237279966,-0.325377428200849,0.983689509218169));
#4219=CARTESIAN_POINT('Origin',(-0.750000000000001,-0.433012701892219,1.));
#4220=CARTESIAN_POINT('',(-0.750000000000001,-0.433012701892219,1.));
#4221=CARTESIAN_POINT('Origin',(0.75,-0.433012701892219,2.));
#4222=CARTESIAN_POINT('',(0.75,-0.433012701892219,2.));
#4223=CARTESIAN_POINT('',(1.38777878078145E-16,-0.866025403784439,2.));
#4224=CARTESIAN_POINT('Origin',(0.75,0.433012701892219,2.));
#4225=CARTESIAN_POINT('',(0.75,0.433012701892219,2.));
#4226=CARTESIAN_POINT('Origin',(0.,0.866025403784439,2.));
#4227=CARTESIAN_POINT('',(1.73472347597681E-17,0.866025403784439,2.));
#4228=CARTESIAN_POINT('Origin',(-0.75,0.43301270189222,2.));
#4229=CARTESIAN_POINT('',(-0.75,0.43301270189222,2.));
#4230=CARTESIAN_POINT('Origin',(-0.750000000000001,-0.433012701892219,2.));
#4231=CARTESIAN_POINT('',(-0.750000000000001,-0.433012701892219,2.));
#4232=CARTESIAN_POINT('Origin',(1.38777878078145E-16,-0.866025403784439,
2.));
#4233=CARTESIAN_POINT('Origin',(2.65969127678468E-15,0.,-2.50000000000012));
#4234=CARTESIAN_POINT('',(0.96675,1.1839272930757E-16,-2.35150733091162E-13));
#4235=CARTESIAN_POINT('',(0.966750000000003,-1.1839272930757E-16,-2.50000000000012));
#4236=CARTESIAN_POINT('Origin',(2.48491185144619E-28,0.,-2.35922392732846E-13));
#4237=CARTESIAN_POINT('Origin',(5.27355936696949E-15,0.,-5.));
#4238=CARTESIAN_POINT('Origin',(-0.999999999999996,0.,-2.37147131571737E-13));
#4972=UNCERTAINTY_MEASURE_WITH_UNIT(LENGTH_MEASURE(0.01),#4995,
'DISTANCE_ACCURACY_VALUE',
'Maximum model space distance between geometric entities at asserted c
onnectivities');
#4982=UNCERTAINTY_MEASURE_WITH_UNIT(LENGTH_MEASURE(0.01),#4995,
'DISTANCE_ACCURACY_VALUE',
'Maximum model space distance between geometric entities at asserted c
onnectivities');
#4984=(
GEOMETRIC_REPRESENTATION_CONTEXT(3)
GLOBAL_UNCERTAINTY_ASSIGNED_CONTEXT((#4972))
GLOBAL_UNIT_ASSIGNED_CONTEXT((#4995,#4997,#4998))
REPRESENTATION_CONTEXT('','3D')
);
#4994=(
GEOMETRIC_REPRESENTATION_CONTEXT(3)
GLOBAL_UNCERTAINTY_ASSIGNED_CONTEXT((#4982))
GLOBAL_UNIT_ASSIGNED_CONTEXT((#4995,#4997,#4998))
REPRESENTATION_CONTEXT('','3D')
);
#4995=(
LENGTH_UNIT()
NAMED_UNIT(*)
SI_UNIT(.MILLI.,.METRE.)
);
#4997=(
NAMED_UNIT(*)
PLANE_ANGLE_UNIT()
SI_UNIT($,.RADIAN.)
);
#4998=(
NAMED_UNIT(*)
SI_UNIT($,.STERADIAN.)
SOLID_ANGLE_UNIT()
);
#5000=SHAPE_DEFINITION_REPRESENTATION(#5011,#5032);
#5011=PRODUCT_DEFINITION_SHAPE('',$,#5044);
#5032=SHAPE_REPRESENTATION('',(#3033),#4984);
#5042=PRODUCT_DEFINITION_CONTEXT('part definition',#5077,'design');
#5044=PRODUCT_DEFINITION(
'BSHCS ASME B18.3.1M - M2x0.4 x 5 Steel Grade 2 Plain','Screw_01',#5055,
#5042);
#5055=PRODUCT_DEFINITION_FORMATION('',$,#5080);
#5077=APPLICATION_CONTEXT(
'Core Data for Automotive Mechanical Design Process');
#5078=PRODUCT_CONTEXT('part definition',#5077,'mechanical');
#5080=PRODUCT('BSHCS ASME B18.3.1M - M2x0.4 x 5 Steel Grade 2 Plain',
'Screw_01',
'Broached Hexagon Socket Head Cap Screw ASME B18.3.1M - M2x0.4 x 5',(#5078));
#5091=PRESENTATION_STYLE_ASSIGNMENT((#5096));
#5096=SURFACE_STYLE_USAGE(.BOTH.,#5101);
#5101=SURFACE_SIDE_STYLE('',(#5106));
#5106=SURFACE_STYLE_FILL_AREA(#5111);
#5111=FILL_AREA_STYLE('Opaque(160,160,160)',(#5116));
#5116=FILL_AREA_STYLE_COLOUR('Opaque(160,160,160)',#5121);
#5121=COLOUR_RGB('Opaque(160,160,160)', 0.09019608, 0.27058824, 0.51372549);
ENDSEC;
END-ISO-10303-21;
